ISO-10303-21;
HEADER;
FILE_DESCRIPTION (('STEP AP214'),
    '1' );
FILE_NAME ('Part3.step',
    '2026-10-09T16:01:55',
    ( '' ),
    ( '' ),
    'SwSTEP 2.0',
    'SolidWorks 2024',
    '' );
FILE_SCHEMA (( 'AUTOMOTIVE_DESIGN' ));
ENDSEC;

DATA;
#18=CIRCLE ( 'NONE', #40620, 8.300000000000002487 ) ;
#85=ORIENTED_EDGE ( 'NONE', *, *, #57080, .T. ) ;
#151=DIRECTION ( 'NONE',  ( 1.000000000000000000, 0.000000000000000000, 0.000000000000000000 ) ) ;
#408=CIRCLE ( 'NONE', #10596, 6.000000000000005329 ) ;
#684=MECHANICAL_DESIGN_GEOMETRIC_PRESENTATION_REPRESENTATION('',(#62800),#8420);
#700=AXIS2_PLACEMENT_3D ( 'NONE', #18899, #62020, #12531 ) ;
#913=AXIS2_PLACEMENT_3D ( 'NONE', #51344, #30135, #56304 ) ;
#1003=AXIS2_PLACEMENT_3D ( 'NONE', #69133, #46856, #24949 ) ;
#1008=SURFACE_STYLE_USAGE ( .BOTH. , #66721 ) ;
#1139=CIRCLE ( 'NONE', #58734, 9.300000000000002487 ) ;
#1340=SURFACE_STYLE_FILL_AREA ( #17933 ) ;
#1573=DIRECTION ( 'NONE',  ( 0.000000000000000000, 0.000000000000000000, 1.000000000000000000 ) ) ;
#1812=EDGE_LOOP ( 'NONE', ( #21750, #12453, #4821, #46142 ) ) ;
#1964=DIRECTION ( 'NONE',  ( -0.000000000000000000, -0.000000000000000000, -1.000000000000000000 ) ) ;
#2137=TOROIDAL_SURFACE ( 'NONE', #1003, 8.300000000000006040, 1.000000000000000000 ) ;
#2201=ORIENTED_EDGE ( 'NONE', *, *, #56952, .T. ) ;
#2252=DIRECTION ( 'NONE',  ( 0.000000000000000000, 0.000000000000000000, 1.000000000000000000 ) ) ;
#2373=ORIENTED_EDGE ( 'NONE', *, *, #47915, .T. ) ;
#2534=CARTESIAN_POINT ( 'NONE',  ( 84.77321854994620765, 47.95351654967443977, 26.00000000000000355 ) ) ;
#2665=ORIENTED_EDGE ( 'NONE', *, *, #59766, .T. ) ;
#2709=EDGE_CURVE ( 'NONE', #52538, #3182, #55696, .T. ) ;
#2730=DIRECTION ( 'NONE',  ( 0.000000000000000000, 0.000000000000000000, 1.000000000000000000 ) ) ;
#2855=DIRECTION ( 'NONE',  ( 1.000000000000000000, 0.000000000000000000, -0.000000000000000000 ) ) ;
#2871=EDGE_CURVE ( 'NONE', #52538, #3728, #14073, .T. ) ;
#2948=CARTESIAN_POINT ( 'NONE',  ( 78.77321854994620765, 47.95351654967443977, 26.00000000000000355 ) ) ;
#3132=CARTESIAN_POINT ( 'NONE',  ( 73.77321854994620765, 47.95351654967443977, 15.00000000000000000 ) ) ;
#3182=VERTEX_POINT ( 'NONE', #26671 ) ;
#3199=ORIENTED_EDGE ( 'NONE', *, *, #57483, .F. ) ;
#3200=ORIENTED_EDGE ( 'NONE', *, *, #59766, .F. ) ;
#3219=DIRECTION ( 'NONE',  ( 0.000000000000000000, 0.000000000000000000, 1.000000000000000000 ) ) ;
#3233=AXIS2_PLACEMENT_3D ( 'NONE', #4580, #53714, #26844 ) ;
#3397=EDGE_CURVE ( 'NONE', #54169, #19545, #33242, .T. ) ;
#3477=FACE_BOUND ( 'NONE', #33256, .T. ) ;
#3728=VERTEX_POINT ( 'NONE', #32856 ) ;
#3848=EDGE_LOOP ( 'NONE', ( #26711, #21221, #61645, #48073 ) ) ;
#3921=CARTESIAN_POINT ( 'NONE',  ( 78.77321854994620765, 47.95351654967443977, 43.00000000000000000 ) ) ;
#4002=TOROIDAL_SURFACE ( 'NONE', #50268, 5.000000000000003553, 1.000000000000000000 ) ;
#4011=EDGE_LOOP ( 'NONE', ( #67663, #22369 ) ) ;
#4012=ORIENTED_EDGE ( 'NONE', *, *, #40364, .F. ) ;
#4328=CARTESIAN_POINT ( 'NONE',  ( 69.47321854994619628, 47.95351654967443977, 40.00000000000000000 ) ) ;
#4474=ORIENTED_EDGE ( 'NONE', *, *, #26056, .F. ) ;
#4580=CARTESIAN_POINT ( 'NONE',  ( 78.77321854994620765, 47.95351654967443977, 20.00000000000000000 ) ) ;
#4589=FACE_OUTER_BOUND ( 'NONE', #29434, .T. ) ;
#4690=CIRCLE ( 'NONE', #46410, 1.000000000000000888 ) ;
#4769=DIRECTION ( 'NONE',  ( -1.000000000000000000, 0.000000000000000000, 0.000000000000000000 ) ) ;
#4818=CARTESIAN_POINT ( 'NONE',  ( 72.77321854994619343, 47.95351654967443977, 26.00000000000000355 ) ) ;
#4821=ORIENTED_EDGE ( 'NONE', *, *, #55596, .T. ) ;
#4890=AXIS2_PLACEMENT_3D ( 'NONE', #44852, #18676, #28250 ) ;
#4954=CARTESIAN_POINT ( 'NONE',  ( 88.07321854994620480, 47.95351654967443977, 40.00000000000000000 ) ) ;
#4989=ORIENTED_EDGE ( 'NONE', *, *, #21980, .T. ) ;
#5097=DIRECTION ( 'NONE',  ( 0.000000000000000000, 0.000000000000000000, 1.000000000000000000 ) ) ;
#5227=CARTESIAN_POINT ( 'NONE',  ( 83.77321854994620765, 47.95351654967443977, 15.00000000000000000 ) ) ;
#5635=ORIENTED_EDGE ( 'NONE', *, *, #37687, .T. ) ;
#5700=CARTESIAN_POINT ( 'NONE',  ( 83.97321854994621049, 47.95351654967443977, 20.00000000000000000 ) ) ;
#5807=CARTESIAN_POINT ( 'NONE',  ( 78.77321854994620765, 47.95351654967443977, 40.00000000000000000 ) ) ;
#5951=CARTESIAN_POINT ( 'NONE',  ( 69.47321854994619628, 47.95351654967443977, 43.00000000000000000 ) ) ;
#6071=AXIS2_PLACEMENT_3D ( 'NONE', #29659, #30374, #13752 ) ;
#6453=ORIENTED_EDGE ( 'NONE', *, *, #69575, .F. ) ;
#6462=( GEOMETRIC_REPRESENTATION_CONTEXT ( 3 ) GLOBAL_UNCERTAINTY_ASSIGNED_CONTEXT ( ( #11137 ) ) GLOBAL_UNIT_ASSIGNED_CONTEXT ( ( #48189, #41121, #14605 ) ) REPRESENTATION_CONTEXT ( 'NONE', 'WORKASPACE' ) );
#6554=CARTESIAN_POINT ( 'NONE',  ( 83.77321854994620765, 47.95351654967443977, 25.00000000000000000 ) ) ;
#6687=DIRECTION ( 'NONE',  ( 1.000000000000000000, 0.000000000000000000, 0.000000000000000000 ) ) ;
#6905=LINE ( 'NONE', #50039, #27852 ) ;
#7007=PRODUCT_DEFINITION_CONTEXT ( 'detailed design', #40428, 'design' ) ;
#7110=EDGE_CURVE ( 'NONE', #67414, #3728, #14917, .T. ) ;
#7383=VECTOR ( 'NONE', #1964, 1000.000000000000000 ) ;
#7462=DIRECTION ( 'NONE',  ( 0.000000000000000000, 0.000000000000000000, 1.000000000000000000 ) ) ;
#7487=DIRECTION ( 'NONE',  ( -0.000000000000000000, -0.000000000000000000, -1.000000000000000000 ) ) ;
#7711=FACE_OUTER_BOUND ( 'NONE', #51297, .T. ) ;
#7726=EDGE_CURVE ( 'NONE', #69042, #55314, #1139, .T. ) ;
#7763=CARTESIAN_POINT ( 'NONE',  ( 78.77321854994620765, 47.95351654967443977, 43.00000000000000000 ) ) ;
#7868=ORIENTED_EDGE ( 'NONE', *, *, #20536, .F. ) ;
#7973=ORIENTED_EDGE ( 'NONE', *, *, #56952, .F. ) ;
#8107=CIRCLE ( 'NONE', #47651, 1.000000000000000888 ) ;
#8122=ADVANCED_FACE ( 'NONE', ( #12510 ), #54635, .T. ) ;
#8213=VERTEX_POINT ( 'NONE', #57048 ) ;
#8420=( GEOMETRIC_REPRESENTATION_CONTEXT ( 3 ) GLOBAL_UNCERTAINTY_ASSIGNED_CONTEXT ( ( #16102 ) ) GLOBAL_UNIT_ASSIGNED_CONTEXT ( ( #29587, #66024, #34882 ) ) REPRESENTATION_CONTEXT ( 'NONE', 'WORKASPACE' ) );
#8440=CARTESIAN_POINT ( 'NONE',  ( 78.77321854994620765, 47.95351654967443977, 15.00000000000000000 ) ) ;
#8678=VECTOR ( 'NONE', #14782, 1000.000000000000000 ) ;
#8686=DIRECTION ( 'NONE',  ( 1.000000000000000000, 0.000000000000000000, 0.000000000000000000 ) ) ;
#8776=PLANE ( 'NONE',  #69970 ) ;
#8945=DIRECTION ( 'NONE',  ( 1.000000000000000000, 0.000000000000000000, 0.000000000000000000 ) ) ;
#9072=CIRCLE ( 'NONE', #48605, 5.000000000000004441 ) ;
#9340=CIRCLE ( 'NONE', #59007, 5.000000000000004441 ) ;
#9449=CARTESIAN_POINT ( 'NONE',  ( 78.77321854994620765, 47.95351654967443977, 25.00000000000000000 ) ) ;
#9724=CARTESIAN_POINT ( 'NONE',  ( 78.77321854994620765, 47.95351654967443977, 29.00000000000000000 ) ) ;
#9856=CIRCLE ( 'NONE', #33606, 6.000000000000005329 ) ;
#9961=DIRECTION ( 'NONE',  ( 1.000000000000000000, 0.000000000000000000, 0.000000000000000000 ) ) ;
#10079=DIRECTION ( 'NONE',  ( -0.000000000000000000, -0.000000000000000000, -1.000000000000000000 ) ) ;
#10209=VECTOR ( 'NONE', #21269, 1000.000000000000000 ) ;
#10345=EDGE_CURVE ( 'NONE', #42153, #59069, #49814, .T. ) ;
#10596=AXIS2_PLACEMENT_3D ( 'NONE', #20916, #15272, #41437 ) ;
#10926=VERTEX_POINT ( 'NONE', #52201 ) ;
#11048=ADVANCED_FACE ( 'NONE', ( #35110 ), #55718, .T. ) ;
#11064=PRODUCT_DEFINITION ( 'UNKNOWN', '', #50510, #7007 ) ;
#11074=DIRECTION ( 'NONE',  ( -1.000000000000000000, 0.000000000000000000, 0.000000000000000000 ) ) ;
#11102=FACE_OUTER_BOUND ( 'NONE', #27352, .T. ) ;
#11137=UNCERTAINTY_MEASURE_WITH_UNIT (LENGTH_MEASURE( 1.000000000000000082E-05 ), #48189, 'distance_accuracy_value', 'NONE');
#11344=DIRECTION ( 'NONE',  ( 0.000000000000000000, -1.000000000000000000, 0.000000000000000000 ) ) ;
#11347=EDGE_CURVE ( 'NONE', #19917, #53316, #36548, .T. ) ;
#11501=DIRECTION ( 'NONE',  ( 1.000000000000000000, 0.000000000000000000, 0.000000000000000000 ) ) ;
#11755=ORIENTED_EDGE ( 'NONE', *, *, #11347, .F. ) ;
#11906=EDGE_CURVE ( 'NONE', #34995, #8213, #69437, .T. ) ;
#12196=DIRECTION ( 'NONE',  ( 0.000000000000000000, 0.000000000000000000, 1.000000000000000000 ) ) ;
#12325=ORIENTED_EDGE ( 'NONE', *, *, #14383, .T. ) ;
#12388=AXIS2_PLACEMENT_3D ( 'NONE', #66274, #29132, #22788 ) ;
#12453=ORIENTED_EDGE ( 'NONE', *, *, #59467, .T. ) ;
#12510=FACE_OUTER_BOUND ( 'NONE', #3848, .T. ) ;
#12531=DIRECTION ( 'NONE',  ( 1.000000000000000000, 0.000000000000000000, 0.000000000000000000 ) ) ;
#12662=CIRCLE ( 'NONE', #31936, 7.300000000000000711 ) ;
#12873=CARTESIAN_POINT ( 'NONE',  ( 78.77321854994620765, 47.95351654967443977, 29.00000000000000000 ) ) ;
#13027=AXIS2_PLACEMENT_3D ( 'NONE', #38833, #60393, #32515 ) ;
#13410=EDGE_CURVE ( 'NONE', #8213, #16525, #26655, .T. ) ;
#13494=CYLINDRICAL_SURFACE ( 'NONE', #19937, 9.300000000000002487 ) ;
#13508=DIRECTION ( 'NONE',  ( 0.000000000000000000, 0.000000000000000000, 1.000000000000000000 ) ) ;
#13752=DIRECTION ( 'NONE',  ( 1.000000000000000000, 0.000000000000000000, 0.000000000000000000 ) ) ;
#13821=ORIENTED_EDGE ( 'NONE', *, *, #17570, .T. ) ;
#13865=FACE_OUTER_BOUND ( 'NONE', #29745, .T. ) ;
#14073=LINE ( 'NONE', #3132, #45484 ) ;
#14324=CARTESIAN_POINT ( 'NONE',  ( 70.47321854994621049, 47.95351654967443977, 40.00000000000000000 ) ) ;
#14383=EDGE_CURVE ( 'NONE', #59069, #42153, #41261, .T. ) ;
#14559=EDGE_CURVE ( 'NONE', #49881, #69042, #49382, .T. ) ;
#14597=CARTESIAN_POINT ( 'NONE',  ( 73.77321854994620765, 47.95351654967443977, 15.00000000000000000 ) ) ;
#14605=( NAMED_UNIT ( * ) SI_UNIT ( $, .STERADIAN. ) SOLID_ANGLE_UNIT ( ) );
#14782=DIRECTION ( 'NONE',  ( -0.000000000000000000, -0.000000000000000000, -1.000000000000000000 ) ) ;
#14917=CIRCLE ( 'NONE', #66822, 5.000000000000004441 ) ;
#15199=DIRECTION ( 'NONE',  ( -0.000000000000000000, -0.000000000000000000, -1.000000000000000000 ) ) ;
#15272=DIRECTION ( 'NONE',  ( 0.000000000000000000, 0.000000000000000000, 1.000000000000000000 ) ) ;
#15386=DIRECTION ( 'NONE',  ( 0.000000000000000000, 0.000000000000000000, 1.000000000000000000 ) ) ;
#15663=DIRECTION ( 'NONE',  ( 1.000000000000000000, 0.000000000000000000, 0.000000000000000000 ) ) ;
#15702=DIRECTION ( 'NONE',  ( -0.1289152302546202611, 1.578756240926647408E-17, 0.9916556173432378163 ) ) ;
#15765=AXIS2_PLACEMENT_3D ( 'NONE', #23626, #45189, #29271 ) ;
#16102=UNCERTAINTY_MEASURE_WITH_UNIT (LENGTH_MEASURE( 1.000000000000000082E-05 ), #29587, 'distance_accuracy_value', 'NONE');
#16116=EDGE_LOOP ( 'NONE', ( #27166, #56349, #12325, #56233 ) ) ;
#16154=CARTESIAN_POINT ( 'NONE',  ( 73.77321854994620765, 47.95351654967443977, 20.00000000000000000 ) ) ;
#16180=ORIENTED_EDGE ( 'NONE', *, *, #13410, .F. ) ;
#16320=EDGE_CURVE ( 'NONE', #34995, #62860, #408, .T. ) ;
#16391=EDGE_CURVE ( 'NONE', #53316, #69042, #27502, .T. ) ;
#16525=VERTEX_POINT ( 'NONE', #56221 ) ;
#16763=DIRECTION ( 'NONE',  ( 0.000000000000000000, 0.000000000000000000, 1.000000000000000000 ) ) ;
#16857=AXIS2_PLACEMENT_3D ( 'NONE', #61752, #40529, #22884 ) ;
#16934=FACE_OUTER_BOUND ( 'NONE', #33896, .T. ) ;
#16967=CARTESIAN_POINT ( 'NONE',  ( 78.77321854994620765, 47.95351654967443977, 40.00000000000000000 ) ) ;
#17570=EDGE_CURVE ( 'NONE', #19917, #55314, #68325, .T. ) ;
#17811=CARTESIAN_POINT ( 'NONE',  ( 83.77321854994620765, 47.95351654967443977, 0.000000000000000000 ) ) ;
#17933=FILL_AREA_STYLE ('',( #55097 ) ) ;
#18095=ADVANCED_FACE ( 'NONE', ( #16934 ), #32240, .T. ) ;
#18115=CYLINDRICAL_SURFACE ( 'NONE', #913, 5.000000000000004441 ) ;
#18160=VERTEX_POINT ( 'NONE', #29607 ) ;
#18548=CARTESIAN_POINT ( 'NONE',  ( 78.77321854994620765, 47.95351654967443977, 0.000000000000000000 ) ) ;
#18676=DIRECTION ( 'NONE',  ( 0.000000000000000000, 0.000000000000000000, 1.000000000000000000 ) ) ;
#18682=ADVANCED_FACE ( 'NONE', ( #19985 ), #52158, .T. ) ;
#18872=ORIENTED_EDGE ( 'NONE', *, *, #16320, .F. ) ;
#18899=CARTESIAN_POINT ( 'NONE',  ( 78.77321854994620765, 47.95351654967443977, 20.00000000000000000 ) ) ;
#19026=CIRCLE ( 'NONE', #3233, 5.200000000000009948 ) ;
#19088=ORIENTED_EDGE ( 'NONE', *, *, #16391, .F. ) ;
#19316=AXIS2_PLACEMENT_3D ( 'NONE', #8440, #61853, #30019 ) ;
#19545=VERTEX_POINT ( 'NONE', #4818 ) ;
#19641=ORIENTED_EDGE ( 'NONE', *, *, #17570, .F. ) ;
#19773=EDGE_CURVE ( 'NONE', #18160, #32104, #52639, .T. ) ;
#19917=VERTEX_POINT ( 'NONE', #68390 ) ;
#19937=AXIS2_PLACEMENT_3D ( 'NONE', #34710, #7487, #44973 ) ;
#19974=FACE_OUTER_BOUND ( 'NONE', #60105, .T. ) ;
#19985=FACE_OUTER_BOUND ( 'NONE', #53067, .T. ) ;
#19993=ORIENTED_EDGE ( 'NONE', *, *, #69575, .T. ) ;
#20087=CARTESIAN_POINT ( 'NONE',  ( 87.07321854994620480, 47.95351654967443977, 39.00000000000000000 ) ) ;
#20141=DIRECTION ( 'NONE',  ( -1.000000000000000000, 0.000000000000000000, 0.000000000000000000 ) ) ;
#20220=DIRECTION ( 'NONE',  ( 1.000000000000000000, 0.000000000000000000, 0.000000000000000000 ) ) ;
#20463=DIRECTION ( 'NONE',  ( -1.000000000000000000, 0.000000000000000000, 0.000000000000000000 ) ) ;
#20536=EDGE_CURVE ( 'NONE', #39955, #49881, #57207, .T. ) ;
#20577=ORIENTED_EDGE ( 'NONE', *, *, #10345, .F. ) ;
#20684=CARTESIAN_POINT ( 'NONE',  ( 78.77321854994620765, 47.95351654967443977, 20.00000000000000000 ) ) ;
#20753=ORIENTED_EDGE ( 'NONE', *, *, #19773, .F. ) ;
#20916=CARTESIAN_POINT ( 'NONE',  ( 78.77321854994620765, 47.95351654967443977, 29.00000000000000000 ) ) ;
#21017=CYLINDRICAL_SURFACE ( 'NONE', #51217, 6.000000000000005329 ) ;
#21173=ADVANCED_FACE ( 'NONE', ( #13865 ), #18115, .T. ) ;
#21221=ORIENTED_EDGE ( 'NONE', *, *, #22900, .T. ) ;
#21269=DIRECTION ( 'NONE',  ( -0.000000000000000000, -0.000000000000000000, -1.000000000000000000 ) ) ;
#21343=CIRCLE ( 'NONE', #23580, 9.300000000000002487 ) ;
#21618=ADVANCED_FACE ( 'NONE', ( #4589 ), #36047, .T. ) ;
#21708=CARTESIAN_POINT ( 'NONE',  ( 78.77321854994620765, 47.95351654967443977, 39.00000000000000000 ) ) ;
#21750=ORIENTED_EDGE ( 'NONE', *, *, #42396, .F. ) ;
#21972=ORIENTED_EDGE ( 'NONE', *, *, #59467, .F. ) ;
#21980=EDGE_CURVE ( 'NONE', #38683, #40165, #26493, .T. ) ;
#22185=ORIENTED_EDGE ( 'NONE', *, *, #19773, .T. ) ;
#22369=ORIENTED_EDGE ( 'NONE', *, *, #57483, .T. ) ;
#22616=DIRECTION ( 'NONE',  ( 0.000000000000000000, 0.000000000000000000, 1.000000000000000000 ) ) ;
#22743=CARTESIAN_POINT ( 'NONE',  ( 78.77321854994620765, 47.95351654967443977, 39.00000000000000000 ) ) ;
#22775=CARTESIAN_POINT ( 'NONE',  ( 0.000000000000000000, 0.000000000000000000, 0.000000000000000000 ) ) ;
#22788=DIRECTION ( 'NONE',  ( -1.000000000000000000, 0.000000000000000000, 0.000000000000000000 ) ) ;
#22884=DIRECTION ( 'NONE',  ( 1.000000000000000000, 0.000000000000000000, -0.000000000000000000 ) ) ;
#22900=EDGE_CURVE ( 'NONE', #62860, #54169, #6905, .T. ) ;
#23210=DIRECTION ( 'NONE',  ( 0.000000000000000000, 0.000000000000000000, 1.000000000000000000 ) ) ;
#23374=AXIS2_PLACEMENT_3D ( 'NONE', #25520, #58031, #9961 ) ;
#23499=PLANE ( 'NONE',  #50765 ) ;
#23571=PLANE ( 'NONE',  #16857 ) ;
#23580=AXIS2_PLACEMENT_3D ( 'NONE', #68788, #58541, #8686 ) ;
#23626=CARTESIAN_POINT ( 'NONE',  ( 78.77321854994620765, 47.95351654967443977, 29.00000000000000000 ) ) ;
#24411=CARTESIAN_POINT ( 'NONE',  ( 78.77321854994620765, 47.95351654967443977, 26.00000000000000355 ) ) ;
#24560=ORIENTED_EDGE ( 'NONE', *, *, #44430, .T. ) ;
#24894=LINE ( 'NONE', #69076, #40808 ) ;
#24949=DIRECTION ( 'NONE',  ( 1.000000000000000000, 0.000000000000000000, 0.000000000000000000 ) ) ;
#25044=FACE_OUTER_BOUND ( 'NONE', #49848, .T. ) ;
#25128=ORIENTED_EDGE ( 'NONE', *, *, #62612, .F. ) ;
#25260=DIRECTION ( 'NONE',  ( 0.000000000000000000, 0.000000000000000000, 1.000000000000000000 ) ) ;
#25285=DIRECTION ( 'NONE',  ( -1.000000000000000000, 0.000000000000000000, 0.000000000000000000 ) ) ;
#25373=AXIS2_PLACEMENT_3D ( 'NONE', #9449, #31387, #52592 ) ;
#25520=CARTESIAN_POINT ( 'NONE',  ( 78.77321854994620765, 47.95351654967443977, 26.00000000000000355 ) ) ;
#25634=DIRECTION ( 'NONE',  ( -0.000000000000000000, -0.000000000000000000, -1.000000000000000000 ) ) ;
#25680=ORIENTED_EDGE ( 'NONE', *, *, #7110, .T. ) ;
#25782=CARTESIAN_POINT ( 'NONE',  ( 78.77321854994620765, 47.95351654967443977, 20.00000000000000000 ) ) ;
#26050=ADVANCED_FACE ( 'NONE', ( #58175 ), #2137, .T. ) ;
#26056=EDGE_CURVE ( 'NONE', #49881, #39955, #21343, .T. ) ;
#26060=ADVANCED_FACE ( 'NONE', ( #46505 ), #63129, .T. ) ;
#26268=FACE_OUTER_BOUND ( 'NONE', #1812, .T. ) ;
#26284=ORIENTED_EDGE ( 'NONE', *, *, #26056, .T. ) ;
#26493=CIRCLE ( 'NONE', #25373, 5.000000000000004441 ) ;
#26655=CIRCLE ( 'NONE', #66154, 7.300000000000000711 ) ;
#26657=CARTESIAN_POINT ( 'NONE',  ( 72.77321854994619343, 47.95351654967443977, 29.00000000000000000 ) ) ;
#26671=CARTESIAN_POINT ( 'NONE',  ( 83.77321854994620765, 47.95351654967443977, 15.00000000000000000 ) ) ;
#26711=ORIENTED_EDGE ( 'NONE', *, *, #37687, .F. ) ;
#26844=DIRECTION ( 'NONE',  ( 1.000000000000000000, 0.000000000000000000, 0.000000000000000000 ) ) ;
#27166=ORIENTED_EDGE ( 'NONE', *, *, #38008, .F. ) ;
#27352=EDGE_LOOP ( 'NONE', ( #11755, #13821, #29596, #19088 ) ) ;
#27502=CIRCLE ( 'NONE', #59155, 1.000000000000000888 ) ;
#27833=ORIENTED_EDGE ( 'NONE', *, *, #28232, .T. ) ;
#27852=VECTOR ( 'NONE', #54670, 1000.000000000000000 ) ;
#28232=EDGE_CURVE ( 'NONE', #38683, #18160, #24894, .T. ) ;
#28250=DIRECTION ( 'NONE',  ( 1.000000000000000000, 0.000000000000000000, 0.000000000000000000 ) ) ;
#28590=EDGE_LOOP ( 'NONE', ( #55195, #38387, #45006, #40335 ) ) ;
#28806=CARTESIAN_POINT ( 'NONE',  ( 78.77321854994620765, 47.95351654967443977, 39.00000000000000000 ) ) ;
#29132=DIRECTION ( 'NONE',  ( -0.000000000000000000, -0.000000000000000000, -1.000000000000000000 ) ) ;
#29264=ORIENTED_EDGE ( 'NONE', *, *, #55596, .F. ) ;
#29271=DIRECTION ( 'NONE',  ( 1.000000000000000000, 0.000000000000000000, 0.000000000000000000 ) ) ;
#29324=DIRECTION ( 'NONE',  ( 1.000000000000000000, 0.000000000000000000, 0.000000000000000000 ) ) ;
#29434=EDGE_LOOP ( 'NONE', ( #3199, #19993, #25680, #65301 ) ) ;
#29467=CARTESIAN_POINT ( 'NONE',  ( 83.97321854994621049, 47.95351654967443977, 15.00000000000000000 ) ) ;
#29587=( LENGTH_UNIT ( ) NAMED_UNIT ( * ) SI_UNIT ( .MILLI., .METRE. ) );
#29596=ORIENTED_EDGE ( 'NONE', *, *, #7726, .F. ) ;
#29607=CARTESIAN_POINT ( 'NONE',  ( 83.77321854994620765, 47.95351654967443977, 20.00000000000000000 ) ) ;
#29659=CARTESIAN_POINT ( 'NONE',  ( 78.77321854994620765, 47.95351654967443977, 39.00000000000000000 ) ) ;
#29745=EDGE_LOOP ( 'NONE', ( #51838, #21972, #85, #63974 ) ) ;
#30019=DIRECTION ( 'NONE',  ( 1.000000000000000000, 0.000000000000000000, 0.000000000000000000 ) ) ;
#30135=DIRECTION ( 'NONE',  ( -0.000000000000000000, -0.000000000000000000, -1.000000000000000000 ) ) ;
#30143=ORIENTED_EDGE ( 'NONE', *, *, #57080, .F. ) ;
#30374=DIRECTION ( 'NONE',  ( -0.000000000000000000, -0.000000000000000000, -1.000000000000000000 ) ) ;
#30498=ORIENTED_EDGE ( 'NONE', *, *, #14383, .F. ) ;
#30603=DIRECTION ( 'NONE',  ( -0.000000000000000000, -0.000000000000000000, -1.000000000000000000 ) ) ;
#30838=EDGE_CURVE ( 'NONE', #16525, #8213, #12662, .T. ) ;
#30925=CYLINDRICAL_SURFACE ( 'NONE', #45503, 5.000000000000004441 ) ;
#31036=LINE ( 'NONE', #5227, #66365 ) ;
#31038=AXIS2_PLACEMENT_3D ( 'NONE', #16967, #22616, #6687 ) ;
#31057=CIRCLE ( 'NONE', #49124, 5.000000000000004441 ) ;
#31075=FACE_OUTER_BOUND ( 'NONE', #16116, .T. ) ;
#31359=ADVANCED_FACE ( 'NONE', ( #11102 ), #48897, .T. ) ;
#31387=DIRECTION ( 'NONE',  ( 0.000000000000000000, 0.000000000000000000, 1.000000000000000000 ) ) ;
#31586=SHAPE_REPRESENTATION_RELATIONSHIP ( 'NONE' , 'NONE' ,  #64796, #34287 ) ;
#31754=LINE ( 'NONE', #40937, #8678 ) ;
#31848=ORIENTED_EDGE ( 'NONE', *, *, #11906, .T. ) ;
#31936=AXIS2_PLACEMENT_3D ( 'NONE', #42309, #63886, #63543 ) ;
#32104=VERTEX_POINT ( 'NONE', #16154 ) ;
#32225=AXIS2_PLACEMENT_3D ( 'NONE', #21708, #5097, #64848 ) ;
#32240=CONICAL_SURFACE ( 'NONE', #13027, 6.000000000000005329, 0.1292750040481423779 ) ;
#32355=DIRECTION ( 'NONE',  ( 1.000000000000000000, 0.000000000000000000, 0.000000000000000000 ) ) ;
#32515=DIRECTION ( 'NONE',  ( 1.000000000000000000, 0.000000000000000000, 0.000000000000000000 ) ) ;
#32856=CARTESIAN_POINT ( 'NONE',  ( 73.77321854994620765, 47.95351654967443977, 0.000000000000000000 ) ) ;
#32957=ORIENTED_EDGE ( 'NONE', *, *, #7726, .T. ) ;
#32980=CARTESIAN_POINT ( 'NONE',  ( 73.77321854994620765, 47.95351654967443977, 26.00000000000000355 ) ) ;
#33242=CIRCLE ( 'NONE', #58128, 6.000000000000005329 ) ;
#33256=EDGE_LOOP ( 'NONE', ( #4012, #20753 ) ) ;
#33419=FACE_OUTER_BOUND ( 'NONE', #42404, .T. ) ;
#33606=AXIS2_PLACEMENT_3D ( 'NONE', #12873, #25260, #68393 ) ;
#33896=EDGE_LOOP ( 'NONE', ( #5635, #31848, #58528, #7973 ) ) ;
#33915=CARTESIAN_POINT ( 'NONE',  ( 73.57321854994619059, 47.95351654967443977, 15.00000000000000000 ) ) ;
#34144=ADVANCED_FACE ( 'NONE', ( #26268 ), #4002, .T. ) ;
#34172=ORIENTED_EDGE ( 'NONE', *, *, #62612, .T. ) ;
#34287=ADVANCED_BREP_SHAPE_REPRESENTATION ( '', ( #44073, #45918 ), #6462 ) ;
#34343=VECTOR ( 'NONE', #15702, 1000.000000000000227 ) ;
#34481=AXIS2_PLACEMENT_3D ( 'NONE', #51172, #2730, #56822 ) ;
#34710=CARTESIAN_POINT ( 'NONE',  ( 78.77321854994620765, 47.95351654967443977, 43.00000000000000000 ) ) ;
#34853=DIRECTION ( 'NONE',  ( 1.000000000000000000, 0.000000000000000000, 0.000000000000000000 ) ) ;
#34882=( NAMED_UNIT ( * ) SI_UNIT ( $, .STERADIAN. ) SOLID_ANGLE_UNIT ( ) );
#34995=VERTEX_POINT ( 'NONE', #65256 ) ;
#35110=FACE_OUTER_BOUND ( 'NONE', #48241, .T. ) ;
#35356=VECTOR ( 'NONE', #56571, 1000.000000000000227 ) ;
#35636=PRODUCT_CONTEXT ( 'NONE', #56227, 'mechanical' ) ;
#35887=DIRECTION ( 'NONE',  ( -1.000000000000000000, 0.000000000000000000, 0.000000000000000000 ) ) ;
#36047=CYLINDRICAL_SURFACE ( 'NONE', #69339, 5.000000000000004441 ) ;
#36084=PLANE ( 'NONE',  #64909 ) ;
#36457=ORIENTED_EDGE ( 'NONE', *, *, #16391, .T. ) ;
#36463=AXIS2_PLACEMENT_3D ( 'NONE', #5807, #16763, #53904 ) ;
#36548=CIRCLE ( 'NONE', #6071, 8.300000000000002487 ) ;
#36605=DIRECTION ( 'NONE',  ( -1.000000000000000000, 0.000000000000000000, 0.000000000000000000 ) ) ;
#36613=ORIENTED_EDGE ( 'NONE', *, *, #14559, .F. ) ;
#36633=AXIS2_PLACEMENT_3D ( 'NONE', #39299, #7462, #44948 ) ;
#36766=ADVANCED_FACE ( 'NONE', ( #50632 ), #13494, .T. ) ;
#36946=CARTESIAN_POINT ( 'NONE',  ( 78.77321854994620765, 47.95351654967443977, 25.00000000000000000 ) ) ;
#37358=ORIENTED_EDGE ( 'NONE', *, *, #2709, .F. ) ;
#37675=AXIS2_PLACEMENT_3D ( 'NONE', #25782, #47332, #20463 ) ;
#37687=EDGE_CURVE ( 'NONE', #62860, #34995, #9856, .T. ) ;
#37740=DIRECTION ( 'NONE',  ( -0.000000000000000000, -0.000000000000000000, -1.000000000000000000 ) ) ;
#38008=EDGE_CURVE ( 'NONE', #10926, #66328, #64128, .T. ) ;
#38119=EDGE_LOOP ( 'NONE', ( #42210, #43676 ) ) ;
#38387=ORIENTED_EDGE ( 'NONE', *, *, #47417, .F. ) ;
#38683=VERTEX_POINT ( 'NONE', #6554 ) ;
#38714=CARTESIAN_POINT ( 'NONE',  ( 78.77321854994620765, 47.95351654967443977, 15.00000000000000000 ) ) ;
#38833=CARTESIAN_POINT ( 'NONE',  ( 78.77321854994620765, 47.95351654967443977, 29.00000000000000000 ) ) ;
#39127=CARTESIAN_POINT ( 'NONE',  ( 78.77321854994620765, 47.95351654967443977, 40.00000000000000000 ) ) ;
#39252=DIRECTION ( 'NONE',  ( 0.000000000000000000, 0.000000000000000000, 1.000000000000000000 ) ) ;
#39299=CARTESIAN_POINT ( 'NONE',  ( 78.77321854994620765, 47.95351654967443977, 25.00000000000000000 ) ) ;
#39744=FACE_BOUND ( 'NONE', #4011, .T. ) ;
#39780=EDGE_LOOP ( 'NONE', ( #41493, #27833, #22185, #30143 ) ) ;
#39955=VERTEX_POINT ( 'NONE', #5951 ) ;
#40165=VERTEX_POINT ( 'NONE', #47266 ) ;
#40335=ORIENTED_EDGE ( 'NONE', *, *, #10345, .T. ) ;
#40364=EDGE_CURVE ( 'NONE', #32104, #18160, #9072, .T. ) ;
#40428=APPLICATION_CONTEXT ( 'automotive_design' ) ;
#40519=EDGE_LOOP ( 'NONE', ( #4474, #45254, #32957, #25128 ) ) ;
#40529=DIRECTION ( 'NONE',  ( 0.000000000000000000, 0.000000000000000000, 1.000000000000000000 ) ) ;
#40620=AXIS2_PLACEMENT_3D ( 'NONE', #22743, #43960, #151 ) ;
#40808=VECTOR ( 'NONE', #46454, 1000.000000000000000 ) ;
#40937=CARTESIAN_POINT ( 'NONE',  ( 73.57321854994619059, 47.95351654967443977, 20.00000000000000000 ) ) ;
#41028=AXIS2_PLACEMENT_3D ( 'NONE', #2948, #2252, #8945 ) ;
#41121=( NAMED_UNIT ( * ) PLANE_ANGLE_UNIT ( ) SI_UNIT ( $, .RADIAN. ) );
#41261=CIRCLE ( 'NONE', #34481, 5.200000000000009948 ) ;
#41408=AXIS2_PLACEMENT_3D ( 'NONE', #7763, #39252, #29324 ) ;
#41437=DIRECTION ( 'NONE',  ( 1.000000000000000000, 0.000000000000000000, 0.000000000000000000 ) ) ;
#41493=ORIENTED_EDGE ( 'NONE', *, *, #21980, .F. ) ;
#41563=FACE_OUTER_BOUND ( 'NONE', #66575, .T. ) ;
#42153=VERTEX_POINT ( 'NONE', #33915 ) ;
#42197=VECTOR ( 'NONE', #15199, 1000.000000000000000 ) ;
#42210=ORIENTED_EDGE ( 'NONE', *, *, #44430, .F. ) ;
#42309=CARTESIAN_POINT ( 'NONE',  ( 78.77321854994620765, 47.95351654967443977, 39.00000000000000000 ) ) ;
#42396=EDGE_CURVE ( 'NONE', #40165, #19545, #4690, .T. ) ;
#42404=EDGE_LOOP ( 'NONE', ( #20577, #30498 ) ) ;
#42525=CARTESIAN_POINT ( 'NONE',  ( 78.77321854994620765, 47.95351654967443977, 26.00000000000000355 ) ) ;
#42934=CARTESIAN_POINT ( 'NONE',  ( 73.57321854994619059, 47.95351654967443977, 20.00000000000000000 ) ) ;
#42955=CARTESIAN_POINT ( 'NONE',  ( 78.77321854994620765, 47.95351654967443977, 43.00000000000000000 ) ) ;
#43023=ADVANCED_FACE ( 'NONE', ( #31075 ), #52656, .T. ) ;
#43168=ORIENTED_EDGE ( 'NONE', *, *, #47417, .T. ) ;
#43174=DIRECTION ( 'NONE',  ( 0.000000000000000000, 0.000000000000000000, -1.000000000000000000 ) ) ;
#43494=CARTESIAN_POINT ( 'NONE',  ( 69.47321854994619628, 47.95351654967443977, 43.00000000000000000 ) ) ;
#43676=ORIENTED_EDGE ( 'NONE', *, *, #7110, .F. ) ;
#43878=DIRECTION ( 'NONE',  ( -1.000000000000000000, 0.000000000000000000, 0.000000000000000000 ) ) ;
#43960=DIRECTION ( 'NONE',  ( -0.000000000000000000, -0.000000000000000000, -1.000000000000000000 ) ) ;
#44015=DIRECTION ( 'NONE',  ( 1.000000000000000000, 0.000000000000000000, -0.000000000000000000 ) ) ;
#44073=MANIFOLD_SOLID_BREP ( 'Fillet1', #69094 ) ;
#44106=EDGE_LOOP ( 'NONE', ( #44681, #69837 ) ) ;
#44180=LINE ( 'NONE', #43494, #49316 ) ;
#44231=ORIENTED_EDGE ( 'NONE', *, *, #22900, .F. ) ;
#44430=EDGE_CURVE ( 'NONE', #3728, #67414, #31057, .T. ) ;
#44681=ORIENTED_EDGE ( 'NONE', *, *, #48403, .T. ) ;
#44707=ADVANCED_FACE ( 'NONE', ( #48582, #48237 ), #53898, .F. ) ;
#44852=CARTESIAN_POINT ( 'NONE',  ( 78.77321854994620765, 47.95351654967443977, 15.00000000000000000 ) ) ;
#44907=AXIS2_PLACEMENT_3D ( 'NONE', #46038, #13508, #67610 ) ;
#44948=DIRECTION ( 'NONE',  ( 1.000000000000000000, 0.000000000000000000, 0.000000000000000000 ) ) ;
#44973=DIRECTION ( 'NONE',  ( -1.000000000000000000, 0.000000000000000000, 0.000000000000000000 ) ) ;
#45006=ORIENTED_EDGE ( 'NONE', *, *, #68521, .T. ) ;
#45148=PRESENTATION_STYLE_ASSIGNMENT (( #1008 ) ) ;
#45189=DIRECTION ( 'NONE',  ( 0.000000000000000000, 0.000000000000000000, 1.000000000000000000 ) ) ;
#45254=ORIENTED_EDGE ( 'NONE', *, *, #14559, .T. ) ;
#45484=VECTOR ( 'NONE', #52265, 1000.000000000000000 ) ;
#45503=AXIS2_PLACEMENT_3D ( 'NONE', #36946, #25634, #43878 ) ;
#45598=CARTESIAN_POINT ( 'NONE',  ( 88.07321854994620480, 47.95351654967443977, 43.00000000000000000 ) ) ;
#45746=EDGE_CURVE ( 'NONE', #19545, #54169, #47057, .T. ) ;
#45918=AXIS2_PLACEMENT_3D ( 'NONE', #22775, #53934, #32355 ) ;
#45968=CARTESIAN_POINT ( 'NONE',  ( 84.77321854994620765, 47.95351654967443977, 29.00000000000000000 ) ) ;
#46006=ORIENTED_EDGE ( 'NONE', *, *, #48403, .F. ) ;
#46038=CARTESIAN_POINT ( 'NONE',  ( 78.77321854994620765, 47.95351654967443977, 20.00000000000000000 ) ) ;
#46142=ORIENTED_EDGE ( 'NONE', *, *, #45746, .F. ) ;
#46247=DIRECTION ( 'NONE',  ( 1.000000000000000000, 0.000000000000000000, -0.000000000000000000 ) ) ;
#46342=FACE_OUTER_BOUND ( 'NONE', #51748, .T. ) ;
#46409=PRODUCT_DEFINITION_SHAPE ( 'NONE', 'NONE',  #11064 ) ;
#46410=AXIS2_PLACEMENT_3D ( 'NONE', #32980, #49253, #11074 ) ;
#46454=DIRECTION ( 'NONE',  ( -0.000000000000000000, -0.000000000000000000, -1.000000000000000000 ) ) ;
#46505=FACE_OUTER_BOUND ( 'NONE', #28590, .T. ) ;
#46856=DIRECTION ( 'NONE',  ( 0.000000000000000000, 0.000000000000000000, 1.000000000000000000 ) ) ;
#46967=AXIS2_PLACEMENT_3D ( 'NONE', #57455, #10079, #25285 ) ;
#47057=CIRCLE ( 'NONE', #23374, 6.000000000000005329 ) ;
#47266=CARTESIAN_POINT ( 'NONE',  ( 73.77321854994620765, 47.95351654967443977, 25.00000000000000000 ) ) ;
#47305=CARTESIAN_POINT ( 'NONE',  ( 78.77321854994620765, 47.95351654967443977, 20.00000000000000000 ) ) ;
#47332=DIRECTION ( 'NONE',  ( -0.000000000000000000, -0.000000000000000000, -1.000000000000000000 ) ) ;
#47417=EDGE_CURVE ( 'NONE', #66328, #10926, #19026, .T. ) ;
#47421=LINE ( 'NONE', #5700, #10209 ) ;
#47651=AXIS2_PLACEMENT_3D ( 'NONE', #66809, #56218, #50206 ) ;
#47714=CARTESIAN_POINT ( 'NONE',  ( 73.77321854994620765, 47.95351654967443977, 25.00000000000000000 ) ) ;
#47915=EDGE_CURVE ( 'NONE', #34995, #19545, #68839, .T. ) ;
#48073=ORIENTED_EDGE ( 'NONE', *, *, #47915, .F. ) ;
#48189=( LENGTH_UNIT ( ) NAMED_UNIT ( * ) SI_UNIT ( .MILLI., .METRE. ) );
#48237=FACE_BOUND ( 'NONE', #51329, .T. ) ;
#48241=EDGE_LOOP ( 'NONE', ( #4989, #65926, #50953, #29264 ) ) ;
#48403=EDGE_CURVE ( 'NONE', #53316, #19917, #18, .T. ) ;
#48463=VECTOR ( 'NONE', #57866, 1000.000000000000000 ) ;
#48582=FACE_OUTER_BOUND ( 'NONE', #44106, .T. ) ;
#48605=AXIS2_PLACEMENT_3D ( 'NONE', #55352, #12196, #11501 ) ;
#48619=ORIENTED_EDGE ( 'NONE', *, *, #45746, .T. ) ;
#48897=TOROIDAL_SURFACE ( 'NONE', #36463, 8.300000000000006040, 1.000000000000000000 ) ;
#49124=AXIS2_PLACEMENT_3D ( 'NONE', #18548, #60651, #50725 ) ;
#49205=ADVANCED_FACE ( 'NONE', ( #56791 ), #23571, .F. ) ;
#49253=DIRECTION ( 'NONE',  ( 1.224646799147353207E-16, 1.000000000000000000, -0.000000000000000000 ) ) ;
#49316=VECTOR ( 'NONE', #53782, 1000.000000000000000 ) ;
#49382=LINE ( 'NONE', #49706, #7383 ) ;
#49621=CONICAL_SURFACE ( 'NONE', #15765, 6.000000000000005329, 0.1292750040481423779 ) ;
#49706=CARTESIAN_POINT ( 'NONE',  ( 88.07321854994620480, 47.95351654967443977, 43.00000000000000000 ) ) ;
#49814=CIRCLE ( 'NONE', #19316, 5.200000000000009948 ) ;
#49848=EDGE_LOOP ( 'NONE', ( #43168, #50492 ) ) ;
#49881=VERTEX_POINT ( 'NONE', #45598 ) ;
#50039=CARTESIAN_POINT ( 'NONE',  ( 84.77321854994620765, 47.95351654967443977, 29.00000000000000000 ) ) ;
#50206=DIRECTION ( 'NONE',  ( 0.000000000000000000, 0.000000000000000000, -1.000000000000000000 ) ) ;
#50268=AXIS2_PLACEMENT_3D ( 'NONE', #42525, #64117, #15663 ) ;
#50382=DIRECTION ( 'NONE',  ( 0.000000000000000000, 0.000000000000000000, 1.000000000000000000 ) ) ;
#50492=ORIENTED_EDGE ( 'NONE', *, *, #38008, .T. ) ;
#50510=PRODUCT_DEFINITION_FORMATION_WITH_SPECIFIED_SOURCE ( 'ANY', '', #57140, .NOT_KNOWN. ) ;
#50632=FACE_OUTER_BOUND ( 'NONE', #40519, .T. ) ;
#50725=DIRECTION ( 'NONE',  ( 1.000000000000000000, 0.000000000000000000, 0.000000000000000000 ) ) ;
#50765=AXIS2_PLACEMENT_3D ( 'NONE', #38714, #1573, #44015 ) ;
#50953=ORIENTED_EDGE ( 'NONE', *, *, #3397, .F. ) ;
#51172=CARTESIAN_POINT ( 'NONE',  ( 78.77321854994620765, 47.95351654967443977, 15.00000000000000000 ) ) ;
#51217=AXIS2_PLACEMENT_3D ( 'NONE', #9724, #68770, #4769 ) ;
#51277=ORIENTED_EDGE ( 'NONE', *, *, #11906, .F. ) ;
#51297=EDGE_LOOP ( 'NONE', ( #51277, #55516, #2201, #16180 ) ) ;
#51329=EDGE_LOOP ( 'NONE', ( #59462, #58440 ) ) ;
#51344=CARTESIAN_POINT ( 'NONE',  ( 78.77321854994620765, 47.95351654967443977, 25.00000000000000000 ) ) ;
#51402=DIRECTION ( 'NONE',  ( 0.000000000000000000, 0.000000000000000000, 1.000000000000000000 ) ) ;
#51748=EDGE_LOOP ( 'NONE', ( #66687, #26284 ) ) ;
#51809=DIRECTION ( 'NONE',  ( 1.000000000000000000, 0.000000000000000000, 0.000000000000000000 ) ) ;
#51838=ORIENTED_EDGE ( 'NONE', *, *, #28232, .F. ) ;
#52158=CYLINDRICAL_SURFACE ( 'NONE', #46967, 5.000000000000004441 ) ;
#52174=DIRECTION ( 'NONE',  ( -0.000000000000000000, -0.000000000000000000, -1.000000000000000000 ) ) ;
#52201=CARTESIAN_POINT ( 'NONE',  ( 83.97321854994621049, 47.95351654967443977, 20.00000000000000000 ) ) ;
#52265=DIRECTION ( 'NONE',  ( -0.000000000000000000, -0.000000000000000000, -1.000000000000000000 ) ) ;
#52538=VERTEX_POINT ( 'NONE', #14597 ) ;
#52592=DIRECTION ( 'NONE',  ( 1.000000000000000000, 0.000000000000000000, 0.000000000000000000 ) ) ;
#52639=CIRCLE ( 'NONE', #700, 5.000000000000004441 ) ;
#52656=CYLINDRICAL_SURFACE ( 'NONE', #37675, 5.200000000000009948 ) ;
#52868=AXIS2_PLACEMENT_3D ( 'NONE', #42955, #52174, #64539 ) ;
#53067=EDGE_LOOP ( 'NONE', ( #6453, #37358, #59993, #24560 ) ) ;
#53239=ADVANCED_FACE ( 'NONE', ( #7711 ), #49621, .T. ) ;
#53316=VERTEX_POINT ( 'NONE', #20087 ) ;
#53319=ADVANCED_FACE ( 'NONE', ( #3477, #25044 ), #8776, .T. ) ;
#53579=ADVANCED_FACE ( 'NONE', ( #39744, #33419 ), #23499, .F. ) ;
#53714=DIRECTION ( 'NONE',  ( 0.000000000000000000, 0.000000000000000000, 1.000000000000000000 ) ) ;
#53782=DIRECTION ( 'NONE',  ( -0.000000000000000000, -0.000000000000000000, -1.000000000000000000 ) ) ;
#53898=PLANE ( 'NONE',  #32225 ) ;
#53904=DIRECTION ( 'NONE',  ( 1.000000000000000000, 0.000000000000000000, 0.000000000000000000 ) ) ;
#53934=DIRECTION ( 'NONE',  ( 0.000000000000000000, 0.000000000000000000, 1.000000000000000000 ) ) ;
#54169=VERTEX_POINT ( 'NONE', #2534 ) ;
#54322=EDGE_CURVE ( 'NONE', #10926, #59069, #47421, .T. ) ;
#54635=CYLINDRICAL_SURFACE ( 'NONE', #12388, 6.000000000000005329 ) ;
#54670=DIRECTION ( 'NONE',  ( -0.000000000000000000, -0.000000000000000000, -1.000000000000000000 ) ) ;
#55097=FILL_AREA_STYLE_COLOUR ( '', #65038 ) ;
#55195=ORIENTED_EDGE ( 'NONE', *, *, #54322, .F. ) ;
#55314=VERTEX_POINT ( 'NONE', #4328 ) ;
#55352=CARTESIAN_POINT ( 'NONE',  ( 78.77321854994620765, 47.95351654967443977, 20.00000000000000000 ) ) ;
#55516=ORIENTED_EDGE ( 'NONE', *, *, #16320, .T. ) ;
#55596=EDGE_CURVE ( 'NONE', #38683, #54169, #8107, .T. ) ;
#55663=CARTESIAN_POINT ( 'NONE',  ( 78.77321854994620765, 47.95351654967443977, 0.000000000000000000 ) ) ;
#55696=CIRCLE ( 'NONE', #4890, 5.000000000000004441 ) ;
#55718=TOROIDAL_SURFACE ( 'NONE', #41028, 5.000000000000003553, 1.000000000000000000 ) ;
#56218=DIRECTION ( 'NONE',  ( 0.000000000000000000, -1.000000000000000000, 0.000000000000000000 ) ) ;
#56221=CARTESIAN_POINT ( 'NONE',  ( 86.07321854994620480, 47.95351654967443977, 39.00000000000000000 ) ) ;
#56227=APPLICATION_CONTEXT ( 'automotive_design' ) ;
#56233=ORIENTED_EDGE ( 'NONE', *, *, #68521, .F. ) ;
#56304=DIRECTION ( 'NONE',  ( -1.000000000000000000, 0.000000000000000000, 0.000000000000000000 ) ) ;
#56349=ORIENTED_EDGE ( 'NONE', *, *, #54322, .T. ) ;
#56571=DIRECTION ( 'NONE',  ( 0.1289152302546202611, 0.000000000000000000, 0.9916556173432378163 ) ) ;
#56685=ADVANCED_FACE ( 'NONE', ( #57789 ), #30925, .T. ) ;
#56791=FACE_OUTER_BOUND ( 'NONE', #38119, .T. ) ;
#56822=DIRECTION ( 'NONE',  ( 1.000000000000000000, 0.000000000000000000, 0.000000000000000000 ) ) ;
#56952=EDGE_CURVE ( 'NONE', #62860, #16525, #57623, .T. ) ;
#57048=CARTESIAN_POINT ( 'NONE',  ( 71.47321854994621049, 47.95351654967443977, 39.00000000000000000 ) ) ;
#57080=EDGE_CURVE ( 'NONE', #40165, #32104, #69646, .T. ) ;
#57140=PRODUCT ( 'Part3', 'Part3', '', ( #35636 ) ) ;
#57207=CIRCLE ( 'NONE', #41408, 9.300000000000002487 ) ;
#57212=DIRECTION ( 'NONE',  ( 0.000000000000000000, 0.000000000000000000, 1.000000000000000000 ) ) ;
#57455=CARTESIAN_POINT ( 'NONE',  ( 78.77321854994620765, 47.95351654967443977, 15.00000000000000000 ) ) ;
#57483=EDGE_CURVE ( 'NONE', #3182, #52538, #9340, .T. ) ;
#57620=CARTESIAN_POINT ( 'NONE',  ( 78.77321854994620765, 47.95351654967443977, 15.00000000000000000 ) ) ;
#57623=LINE ( 'NONE', #45968, #35356 ) ;
#57789=FACE_OUTER_BOUND ( 'NONE', #39780, .T. ) ;
#57866=DIRECTION ( 'NONE',  ( -0.000000000000000000, -0.000000000000000000, -1.000000000000000000 ) ) ;
#57912=EDGE_LOOP ( 'NONE', ( #19641, #46006, #36457, #3200 ) ) ;
#58031=DIRECTION ( 'NONE',  ( 0.000000000000000000, 0.000000000000000000, 1.000000000000000000 ) ) ;
#58128=AXIS2_PLACEMENT_3D ( 'NONE', #24411, #67190, #62230 ) ;
#58175=FACE_OUTER_BOUND ( 'NONE', #57912, .T. ) ;
#58440=ORIENTED_EDGE ( 'NONE', *, *, #13410, .T. ) ;
#58528=ORIENTED_EDGE ( 'NONE', *, *, #30838, .F. ) ;
#58541=DIRECTION ( 'NONE',  ( 0.000000000000000000, 0.000000000000000000, 1.000000000000000000 ) ) ;
#58542=CYLINDRICAL_SURFACE ( 'NONE', #52868, 9.300000000000002487 ) ;
#58734=AXIS2_PLACEMENT_3D ( 'NONE', #39127, #23210, #34853 ) ;
#59007=AXIS2_PLACEMENT_3D ( 'NONE', #63824, #15386, #51809 ) ;
#59069=VERTEX_POINT ( 'NONE', #29467 ) ;
#59155=AXIS2_PLACEMENT_3D ( 'NONE', #59792, #11344, #43174 ) ;
#59462=ORIENTED_EDGE ( 'NONE', *, *, #30838, .T. ) ;
#59467=EDGE_CURVE ( 'NONE', #40165, #38683, #67111, .T. ) ;
#59552=ADVANCED_FACE ( 'NONE', ( #46342 ), #36084, .T. ) ;
#59766=EDGE_CURVE ( 'NONE', #55314, #69042, #61494, .T. ) ;
#59792=CARTESIAN_POINT ( 'NONE',  ( 87.07321854994620480, 47.95351654967443977, 40.00000000000000000 ) ) ;
#59993=ORIENTED_EDGE ( 'NONE', *, *, #2871, .T. ) ;
#60105=EDGE_LOOP ( 'NONE', ( #44231, #18872, #2373, #48619 ) ) ;
#60393=DIRECTION ( 'NONE',  ( 0.000000000000000000, 0.000000000000000000, 1.000000000000000000 ) ) ;
#60651=DIRECTION ( 'NONE',  ( 0.000000000000000000, 0.000000000000000000, 1.000000000000000000 ) ) ;
#61494=CIRCLE ( 'NONE', #31038, 9.300000000000002487 ) ;
#61645=ORIENTED_EDGE ( 'NONE', *, *, #3397, .T. ) ;
#61752=CARTESIAN_POINT ( 'NONE',  ( 78.77321854994620765, 47.95351654967443977, 0.000000000000000000 ) ) ;
#61853=DIRECTION ( 'NONE',  ( 0.000000000000000000, 0.000000000000000000, 1.000000000000000000 ) ) ;
#61948=AXIS2_PLACEMENT_3D ( 'NONE', #20684, #30603, #36605 ) ;
#62020=DIRECTION ( 'NONE',  ( 0.000000000000000000, 0.000000000000000000, 1.000000000000000000 ) ) ;
#62230=DIRECTION ( 'NONE',  ( 1.000000000000000000, 0.000000000000000000, 0.000000000000000000 ) ) ;
#62612=EDGE_CURVE ( 'NONE', #39955, #55314, #44180, .T. ) ;
#62800=STYLED_ITEM ( 'NONE', ( #45148 ), #44073 ) ;
#62860=VERTEX_POINT ( 'NONE', #66787 ) ;
#63129=CYLINDRICAL_SURFACE ( 'NONE', #61948, 5.200000000000009948 ) ;
#63175=CARTESIAN_POINT ( 'NONE',  ( 72.77321854994619343, 47.95351654967443977, 29.00000000000000000 ) ) ;
#63543=DIRECTION ( 'NONE',  ( 1.000000000000000000, 0.000000000000000000, 0.000000000000000000 ) ) ;
#63824=CARTESIAN_POINT ( 'NONE',  ( 78.77321854994620765, 47.95351654967443977, 15.00000000000000000 ) ) ;
#63886=DIRECTION ( 'NONE',  ( 0.000000000000000000, 0.000000000000000000, 1.000000000000000000 ) ) ;
#63974=ORIENTED_EDGE ( 'NONE', *, *, #40364, .T. ) ;
#64117=DIRECTION ( 'NONE',  ( 0.000000000000000000, 0.000000000000000000, 1.000000000000000000 ) ) ;
#64128=CIRCLE ( 'NONE', #44907, 5.200000000000009948 ) ;
#64539=DIRECTION ( 'NONE',  ( -1.000000000000000000, 0.000000000000000000, 0.000000000000000000 ) ) ;
#64796=SHAPE_REPRESENTATION ( 'Part3', ( #45918 ), #6462 ) ;
#64848=DIRECTION ( 'NONE',  ( 1.000000000000000000, 0.000000000000000000, -0.000000000000000000 ) ) ;
#64909=AXIS2_PLACEMENT_3D ( 'NONE', #3921, #3219, #2855 ) ;
#65038=COLOUR_RGB ( '', 0.72549020, 0.75294118, 0.79215686) ;
#65256=CARTESIAN_POINT ( 'NONE',  ( 72.77321854994619343, 47.95351654967443977, 29.00000000000000000 ) ) ;
#65301=ORIENTED_EDGE ( 'NONE', *, *, #2871, .F. ) ;
#65926=ORIENTED_EDGE ( 'NONE', *, *, #42396, .T. ) ;
#66024=( NAMED_UNIT ( * ) PLANE_ANGLE_UNIT ( ) SI_UNIT ( $, .RADIAN. ) );
#66154=AXIS2_PLACEMENT_3D ( 'NONE', #28806, #50382, #20220 ) ;
#66274=CARTESIAN_POINT ( 'NONE',  ( 78.77321854994620765, 47.95351654967443977, 29.00000000000000000 ) ) ;
#66276=ADVANCED_FACE ( 'NONE', ( #19974 ), #21017, .T. ) ;
#66328=VERTEX_POINT ( 'NONE', #42934 ) ;
#66365=VECTOR ( 'NONE', #37740, 1000.000000000000000 ) ;
#66575=EDGE_LOOP ( 'NONE', ( #36613, #7868, #34172, #2665 ) ) ;
#66687=ORIENTED_EDGE ( 'NONE', *, *, #20536, .T. ) ;
#66721=SURFACE_SIDE_STYLE ('',( #1340 ) ) ;
#66787=CARTESIAN_POINT ( 'NONE',  ( 84.77321854994620765, 47.95351654967443977, 29.00000000000000000 ) ) ;
#66809=CARTESIAN_POINT ( 'NONE',  ( 83.77321854994620765, 47.95351654967443977, 26.00000000000000355 ) ) ;
#66822=AXIS2_PLACEMENT_3D ( 'NONE', #55663, #51402, #66959 ) ;
#66959=DIRECTION ( 'NONE',  ( 1.000000000000000000, 0.000000000000000000, 0.000000000000000000 ) ) ;
#67111=CIRCLE ( 'NONE', #36633, 5.000000000000004441 ) ;
#67190=DIRECTION ( 'NONE',  ( 0.000000000000000000, 0.000000000000000000, 1.000000000000000000 ) ) ;
#67414=VERTEX_POINT ( 'NONE', #17811 ) ;
#67610=DIRECTION ( 'NONE',  ( 1.000000000000000000, 0.000000000000000000, 0.000000000000000000 ) ) ;
#67663=ORIENTED_EDGE ( 'NONE', *, *, #2709, .T. ) ;
#68325=CIRCLE ( 'NONE', #69442, 1.000000000000000888 ) ;
#68390=CARTESIAN_POINT ( 'NONE',  ( 70.47321854994621049, 47.95351654967443977, 39.00000000000000000 ) ) ;
#68393=DIRECTION ( 'NONE',  ( 1.000000000000000000, 0.000000000000000000, 0.000000000000000000 ) ) ;
#68521=EDGE_CURVE ( 'NONE', #66328, #42153, #31754, .T. ) ;
#68538=SHAPE_DEFINITION_REPRESENTATION ( #46409, #64796 ) ;
#68590=DIRECTION ( 'NONE',  ( -0.000000000000000000, -0.000000000000000000, -1.000000000000000000 ) ) ;
#68766=DIRECTION ( 'NONE',  ( 1.224646799147353207E-16, 1.000000000000000000, -0.000000000000000000 ) ) ;
#68770=DIRECTION ( 'NONE',  ( -0.000000000000000000, -0.000000000000000000, -1.000000000000000000 ) ) ;
#68788=CARTESIAN_POINT ( 'NONE',  ( 78.77321854994620765, 47.95351654967443977, 43.00000000000000000 ) ) ;
#68839=LINE ( 'NONE', #63175, #48463 ) ;
#69042=VERTEX_POINT ( 'NONE', #4954 ) ;
#69076=CARTESIAN_POINT ( 'NONE',  ( 83.77321854994620765, 47.95351654967443977, 25.00000000000000000 ) ) ;
#69094=CLOSED_SHELL ( 'NONE', ( #31359, #11048, #36766, #18095, #8122, #56685, #43023, #21618, #18682, #49205, #26060, #53319, #53579, #21173, #66276, #53239, #44707, #69953, #59552, #34144, #26050 ) ) ;
#69133=CARTESIAN_POINT ( 'NONE',  ( 78.77321854994620765, 47.95351654967443977, 40.00000000000000000 ) ) ;
#69339=AXIS2_PLACEMENT_3D ( 'NONE', #57620, #68590, #20141 ) ;
#69437=LINE ( 'NONE', #26657, #34343 ) ;
#69442=AXIS2_PLACEMENT_3D ( 'NONE', #14324, #68766, #35887 ) ;
#69575=EDGE_CURVE ( 'NONE', #3182, #67414, #31036, .T. ) ;
#69646=LINE ( 'NONE', #47714, #42197 ) ;
#69837=ORIENTED_EDGE ( 'NONE', *, *, #11347, .T. ) ;
#69953=ADVANCED_FACE ( 'NONE', ( #41563 ), #58542, .T. ) ;
#69970=AXIS2_PLACEMENT_3D ( 'NONE', #47305, #57212, #46247 ) ;
ENDSEC;
END-ISO-10303-21;
